ISO-10303-21;
HEADER;
/* Generated by software containing ST-Developer
 * from STEP Tools, Inc. (www.steptools.com) 
 */

FILE_DESCRIPTION(
/* description */ ('Cable chain and bracket set'),
/* implementation_level */ '2;1');

FILE_NAME(
/* name */ 'Hex Nut - M6__PD6072.step',
/* time_stamp */ '2026-10-29T17:19:47-07:00',
/* author */ (''),
/* organization */ (''),
/* preprocessor_version */ 'ST-DEVELOPER v20.2',
/* originating_system */ 'Autodesk Translation Framework v15.17.0.0',
/* authorisation */ '');

FILE_SCHEMA (('AUTOMOTIVE_DESIGN { 1 0 10303 214 3 1 1 }'));
ENDSEC;

DATA;
#10=MECHANICAL_DESIGN_GEOMETRIC_PRESENTATION_REPRESENTATION('',(#343),#5929);
#253=(
BOUNDED_CURVE()
B_SPLINE_CURVE(2,(#5273,#5274,#5275),.UNSPECIFIED.,.F.,.F.)
B_SPLINE_CURVE_WITH_KNOTS((3,3),(0.144988513094728,0.791574906712449),
 .UNSPECIFIED.)
CURVE()
GEOMETRIC_REPRESENTATION_ITEM()
RATIONAL_B_SPLINE_CURVE((1.09282032302755,1.26188021535082,1.09282032302931))
REPRESENTATION_ITEM('')
);
#254=(
BOUNDED_CURVE()
B_SPLINE_CURVE(2,(#5277,#5278,#5279),.UNSPECIFIED.,.F.,.F.)
B_SPLINE_CURVE_WITH_KNOTS((3,3),(0.144988513094728,0.791574906712449),
 .UNSPECIFIED.)
CURVE()
GEOMETRIC_REPRESENTATION_ITEM()
RATIONAL_B_SPLINE_CURVE((1.09282032302755,1.26188021535082,1.09282032302931))
REPRESENTATION_ITEM('')
);
#255=(
BOUNDED_CURVE()
B_SPLINE_CURVE(2,(#5284,#5285,#5286),.UNSPECIFIED.,.F.,.F.)
B_SPLINE_CURVE_WITH_KNOTS((3,3),(0.144988513094728,0.791574906712449),
 .UNSPECIFIED.)
CURVE()
GEOMETRIC_REPRESENTATION_ITEM()
RATIONAL_B_SPLINE_CURVE((1.09282032302755,1.26188021535082,1.09282032302931))
REPRESENTATION_ITEM('')
);
#256=(
BOUNDED_CURVE()
B_SPLINE_CURVE(2,(#5288,#5289,#5290),.UNSPECIFIED.,.F.,.F.)
B_SPLINE_CURVE_WITH_KNOTS((3,3),(0.144988513094728,0.791574906712449),
 .UNSPECIFIED.)
CURVE()
GEOMETRIC_REPRESENTATION_ITEM()
RATIONAL_B_SPLINE_CURVE((1.09282032302755,1.26188021535082,1.09282032302931))
REPRESENTATION_ITEM('')
);
#257=(
BOUNDED_CURVE()
B_SPLINE_CURVE(2,(#5292,#5293,#5294),.UNSPECIFIED.,.F.,.F.)
B_SPLINE_CURVE_WITH_KNOTS((3,3),(0.144988513094728,0.791574906712449),
 .UNSPECIFIED.)
CURVE()
GEOMETRIC_REPRESENTATION_ITEM()
RATIONAL_B_SPLINE_CURVE((1.09282032302755,1.26188021535082,1.09282032302931))
REPRESENTATION_ITEM('')
);
#258=(
BOUNDED_CURVE()
B_SPLINE_CURVE(2,(#5295,#5296,#5297),.UNSPECIFIED.,.F.,.F.)
B_SPLINE_CURVE_WITH_KNOTS((3,3),(0.144988513094728,0.791574906712449),
 .UNSPECIFIED.)
CURVE()
GEOMETRIC_REPRESENTATION_ITEM()
RATIONAL_B_SPLINE_CURVE((1.09282032302755,1.26188021535082,1.09282032302931))
REPRESENTATION_ITEM('')
);
#259=(
BOUNDED_CURVE()
B_SPLINE_CURVE(2,(#5304,#5305,#5306),.UNSPECIFIED.,.F.,.F.)
B_SPLINE_CURVE_WITH_KNOTS((3,3),(0.144988513094728,0.791574906712449),
 .UNSPECIFIED.)
CURVE()
GEOMETRIC_REPRESENTATION_ITEM()
RATIONAL_B_SPLINE_CURVE((1.09282032302755,1.26188021535082,1.09282032302931))
REPRESENTATION_ITEM('')
);
#260=(
BOUNDED_CURVE()
B_SPLINE_CURVE(2,(#5308,#5309,#5310),.UNSPECIFIED.,.F.,.F.)
B_SPLINE_CURVE_WITH_KNOTS((3,3),(0.144988513094727,0.791574906712449),
 .UNSPECIFIED.)
CURVE()
GEOMETRIC_REPRESENTATION_ITEM()
RATIONAL_B_SPLINE_CURVE((1.09282032302755,1.26188021535082,1.09282032302931))
REPRESENTATION_ITEM('')
);
#261=(
BOUNDED_CURVE()
B_SPLINE_CURVE(2,(#5312,#5313,#5314),.UNSPECIFIED.,.F.,.F.)
B_SPLINE_CURVE_WITH_KNOTS((3,3),(0.144988513094728,0.791574906712449),
 .UNSPECIFIED.)
CURVE()
GEOMETRIC_REPRESENTATION_ITEM()
RATIONAL_B_SPLINE_CURVE((1.09282032302755,1.26188021535082,1.09282032302931))
REPRESENTATION_ITEM('')
);
#262=(
BOUNDED_CURVE()
B_SPLINE_CURVE(2,(#5316,#5317,#5318),.UNSPECIFIED.,.F.,.F.)
B_SPLINE_CURVE_WITH_KNOTS((3,3),(0.144988513094728,0.791574906712449),
 .UNSPECIFIED.)
CURVE()
GEOMETRIC_REPRESENTATION_ITEM()
RATIONAL_B_SPLINE_CURVE((1.09282032302755,1.26188021535082,1.09282032302931))
REPRESENTATION_ITEM('')
);
#263=(
BOUNDED_CURVE()
B_SPLINE_CURVE(2,(#5320,#5321,#5322),.UNSPECIFIED.,.F.,.F.)
B_SPLINE_CURVE_WITH_KNOTS((3,3),(0.144988513094728,0.791574906712449),
 .UNSPECIFIED.)
CURVE()
GEOMETRIC_REPRESENTATION_ITEM()
RATIONAL_B_SPLINE_CURVE((1.09282032302755,1.26188021535082,1.09282032302931))
REPRESENTATION_ITEM('')
);
#264=(
BOUNDED_CURVE()
B_SPLINE_CURVE(2,(#5323,#5324,#5325),.UNSPECIFIED.,.F.,.F.)
B_SPLINE_CURVE_WITH_KNOTS((3,3),(0.144988513094727,0.791574906712449),
 .UNSPECIFIED.)
CURVE()
GEOMETRIC_REPRESENTATION_ITEM()
RATIONAL_B_SPLINE_CURVE((1.09282032302755,1.26188021535082,1.09282032302931))
REPRESENTATION_ITEM('')
);
#285=CONICAL_SURFACE('',#3576,0.576175134594879,1.0471975511966);
#286=CONICAL_SURFACE('',#3578,0.576175134594879,1.0471975511966);
#317=SHAPE_REPRESENTATION_RELATIONSHIP('SRR','None',#6048,#330);
#330=ADVANCED_BREP_SHAPE_REPRESENTATION('',(#356),#5915);
#343=STYLED_ITEM('',(#6227),#356);
#356=MANIFOLD_SOLID_BREP('Body1',#3337);
#383=FACE_BOUND('',#821,.T.);
#384=FACE_BOUND('',#823,.T.);
#459=PLANE('',#3580);
#460=PLANE('',#3581);
#461=PLANE('',#3582);
#462=PLANE('',#3586);
#463=PLANE('',#3587);
#464=PLANE('',#3588);
#465=PLANE('',#3589);
#466=PLANE('',#3590);
#609=FACE_OUTER_BOUND('',#811,.T.);
#610=FACE_OUTER_BOUND('',#812,.T.);
#611=FACE_OUTER_BOUND('',#813,.T.);
#612=FACE_OUTER_BOUND('',#814,.T.);
#613=FACE_OUTER_BOUND('',#815,.T.);
#614=FACE_OUTER_BOUND('',#816,.T.);
#615=FACE_OUTER_BOUND('',#817,.T.);
#616=FACE_OUTER_BOUND('',#818,.T.);
#617=FACE_OUTER_BOUND('',#819,.T.);
#618=FACE_OUTER_BOUND('',#820,.T.);
#619=FACE_OUTER_BOUND('',#822,.T.);
#811=EDGE_LOOP('',(#2629,#2630,#2631,#2632,#2633,#2634,#2635,#2636,#2637));
#812=EDGE_LOOP('',(#2638,#2639,#2640,#2641,#2642,#2643,#2644,#2645,#2646));
#813=EDGE_LOOP('',(#2647,#2648,#2649,#2650));
#814=EDGE_LOOP('',(#2651,#2652,#2653,#2654));
#815=EDGE_LOOP('',(#2655,#2656,#2657,#2658));
#816=EDGE_LOOP('',(#2659,#2660,#2661,#2662));
#817=EDGE_LOOP('',(#2663,#2664,#2665,#2666));
#818=EDGE_LOOP('',(#2667,#2668,#2669,#2670));
#819=EDGE_LOOP('',(#2671,#2672,#2673,#2674));
#820=EDGE_LOOP('',(#2675));
#821=EDGE_LOOP('',(#2676));
#822=EDGE_LOOP('',(#2677));
#823=EDGE_LOOP('',(#2678));
#1055=LINE('',#5281,#1315);
#1056=LINE('',#5302,#1316);
#1057=LINE('',#5327,#1317);
#1058=LINE('',#5328,#1318);
#1059=LINE('',#5330,#1319);
#1060=LINE('',#5332,#1320);
#1061=LINE('',#5337,#1321);
#1062=LINE('',#5340,#1322);
#1063=LINE('',#5342,#1323);
#1315=VECTOR('',#4246,0.576175134594879);
#1316=VECTOR('',#4253,0.576175134594879);
#1317=VECTOR('',#4256,1.00000000000011);
#1318=VECTOR('',#4257,1.00000000000011);
#1319=VECTOR('',#4260,1.00000000000011);
#1320=VECTOR('',#4263,1.00000000000011);
#1321=VECTOR('',#4268,0.300000000000034);
#1322=VECTOR('',#4273,1.00000000000011);
#1323=VECTOR('',#4276,1.00000000000011);
#1505=CIRCLE('',#3577,0.475000000000054);
#1506=CIRCLE('',#3579,0.475000000000054);
#1507=CIRCLE('',#3584,0.251750000000029);
#1508=CIRCLE('',#3585,0.251750000000029);
#1679=VERTEX_POINT('',#5271);
#1680=VERTEX_POINT('',#5272);
#1681=VERTEX_POINT('',#5276);
#1682=VERTEX_POINT('',#5280);
#1683=VERTEX_POINT('',#5283);
#1684=VERTEX_POINT('',#5287);
#1685=VERTEX_POINT('',#5291);
#1686=VERTEX_POINT('',#5299);
#1687=VERTEX_POINT('',#5301);
#1688=VERTEX_POINT('',#5303);
#1689=VERTEX_POINT('',#5307);
#1690=VERTEX_POINT('',#5311);
#1691=VERTEX_POINT('',#5315);
#1692=VERTEX_POINT('',#5319);
#1693=VERTEX_POINT('',#5334);
#1694=VERTEX_POINT('',#5336);
#2015=EDGE_CURVE('',#1679,#1680,#253,.T.);
#2016=EDGE_CURVE('',#1681,#1679,#254,.T.);
#2017=EDGE_CURVE('',#1681,#1682,#1055,.T.);
#2018=EDGE_CURVE('',#1682,#1682,#1505,.T.);
#2019=EDGE_CURVE('',#1683,#1681,#255,.T.);
#2020=EDGE_CURVE('',#1684,#1683,#256,.T.);
#2021=EDGE_CURVE('',#1685,#1684,#257,.T.);
#2022=EDGE_CURVE('',#1680,#1685,#258,.T.);
#2023=EDGE_CURVE('',#1686,#1686,#1506,.T.);
#2024=EDGE_CURVE('',#1686,#1687,#1056,.T.);
#2025=EDGE_CURVE('',#1688,#1687,#259,.T.);
#2026=EDGE_CURVE('',#1689,#1688,#260,.T.);
#2027=EDGE_CURVE('',#1690,#1689,#261,.T.);
#2028=EDGE_CURVE('',#1691,#1690,#262,.T.);
#2029=EDGE_CURVE('',#1692,#1691,#263,.T.);
#2030=EDGE_CURVE('',#1687,#1692,#264,.T.);
#2031=EDGE_CURVE('',#1683,#1692,#1057,.T.);
#2032=EDGE_CURVE('',#1684,#1691,#1058,.T.);
#2033=EDGE_CURVE('',#1681,#1687,#1059,.T.);
#2034=EDGE_CURVE('',#1679,#1688,#1060,.T.);
#2035=EDGE_CURVE('',#1693,#1693,#1507,.F.);
#2036=EDGE_CURVE('',#1693,#1694,#1061,.T.);
#2037=EDGE_CURVE('',#1694,#1694,#1508,.F.);
#2038=EDGE_CURVE('',#1680,#1689,#1062,.T.);
#2039=EDGE_CURVE('',#1685,#1690,#1063,.T.);
#2629=ORIENTED_EDGE('',*,*,#2015,.F.);
#2630=ORIENTED_EDGE('',*,*,#2016,.F.);
#2631=ORIENTED_EDGE('',*,*,#2017,.T.);
#2632=ORIENTED_EDGE('',*,*,#2018,.F.);
#2633=ORIENTED_EDGE('',*,*,#2017,.F.);
#2634=ORIENTED_EDGE('',*,*,#2019,.F.);
#2635=ORIENTED_EDGE('',*,*,#2020,.F.);
#2636=ORIENTED_EDGE('',*,*,#2021,.F.);
#2637=ORIENTED_EDGE('',*,*,#2022,.F.);
#2638=ORIENTED_EDGE('',*,*,#2023,.F.);
#2639=ORIENTED_EDGE('',*,*,#2024,.T.);
#2640=ORIENTED_EDGE('',*,*,#2025,.F.);
#2641=ORIENTED_EDGE('',*,*,#2026,.F.);
#2642=ORIENTED_EDGE('',*,*,#2027,.F.);
#2643=ORIENTED_EDGE('',*,*,#2028,.F.);
#2644=ORIENTED_EDGE('',*,*,#2029,.F.);
#2645=ORIENTED_EDGE('',*,*,#2030,.F.);
#2646=ORIENTED_EDGE('',*,*,#2024,.F.);
#2647=ORIENTED_EDGE('',*,*,#2020,.T.);
#2648=ORIENTED_EDGE('',*,*,#2031,.T.);
#2649=ORIENTED_EDGE('',*,*,#2029,.T.);
#2650=ORIENTED_EDGE('',*,*,#2032,.F.);
#2651=ORIENTED_EDGE('',*,*,#2019,.T.);
#2652=ORIENTED_EDGE('',*,*,#2033,.T.);
#2653=ORIENTED_EDGE('',*,*,#2030,.T.);
#2654=ORIENTED_EDGE('',*,*,#2031,.F.);
#2655=ORIENTED_EDGE('',*,*,#2016,.T.);
#2656=ORIENTED_EDGE('',*,*,#2034,.T.);
#2657=ORIENTED_EDGE('',*,*,#2025,.T.);
#2658=ORIENTED_EDGE('',*,*,#2033,.F.);
#2659=ORIENTED_EDGE('',*,*,#2035,.F.);
#2660=ORIENTED_EDGE('',*,*,#2036,.T.);
#2661=ORIENTED_EDGE('',*,*,#2037,.T.);
#2662=ORIENTED_EDGE('',*,*,#2036,.F.);
#2663=ORIENTED_EDGE('',*,*,#2015,.T.);
#2664=ORIENTED_EDGE('',*,*,#2038,.T.);
#2665=ORIENTED_EDGE('',*,*,#2026,.T.);
#2666=ORIENTED_EDGE('',*,*,#2034,.F.);
#2667=ORIENTED_EDGE('',*,*,#2021,.T.);
#2668=ORIENTED_EDGE('',*,*,#2032,.T.);
#2669=ORIENTED_EDGE('',*,*,#2028,.T.);
#2670=ORIENTED_EDGE('',*,*,#2039,.F.);
#2671=ORIENTED_EDGE('',*,*,#2022,.T.);
#2672=ORIENTED_EDGE('',*,*,#2039,.T.);
#2673=ORIENTED_EDGE('',*,*,#2027,.T.);
#2674=ORIENTED_EDGE('',*,*,#2038,.F.);
#2675=ORIENTED_EDGE('',*,*,#2023,.T.);
#2676=ORIENTED_EDGE('',*,*,#2035,.T.);
#2677=ORIENTED_EDGE('',*,*,#2018,.T.);
#2678=ORIENTED_EDGE('',*,*,#2037,.F.);
#3123=CYLINDRICAL_SURFACE('',#3583,0.251750000000029);
#3231=ADVANCED_FACE('',(#609),#285,.T.);
#3232=ADVANCED_FACE('',(#610),#286,.T.);
#3233=ADVANCED_FACE('',(#611),#459,.T.);
#3234=ADVANCED_FACE('',(#612),#460,.T.);
#3235=ADVANCED_FACE('',(#613),#461,.T.);
#3236=ADVANCED_FACE('',(#614),#3123,.F.);
#3237=ADVANCED_FACE('',(#615),#462,.T.);
#3238=ADVANCED_FACE('',(#616),#463,.T.);
#3239=ADVANCED_FACE('',(#617),#464,.T.);
#3240=ADVANCED_FACE('',(#618,#383),#465,.T.);
#3241=ADVANCED_FACE('',(#619,#384),#466,.F.);
#3337=CLOSED_SHELL('',(#3231,#3232,#3233,#3234,#3235,#3236,#3237,#3238,
#3239,#3240,#3241));
#3575=AXIS2_PLACEMENT_3D('',#5269,#4242,#4243);
#3576=AXIS2_PLACEMENT_3D('',#5270,#4244,#4245);
#3577=AXIS2_PLACEMENT_3D('',#5282,#4247,#4248);
#3578=AXIS2_PLACEMENT_3D('',#5298,#4249,#4250);
#3579=AXIS2_PLACEMENT_3D('',#5300,#4251,#4252);
#3580=AXIS2_PLACEMENT_3D('',#5326,#4254,#4255);
#3581=AXIS2_PLACEMENT_3D('',#5329,#4258,#4259);
#3582=AXIS2_PLACEMENT_3D('',#5331,#4261,#4262);
#3583=AXIS2_PLACEMENT_3D('',#5333,#4264,#4265);
#3584=AXIS2_PLACEMENT_3D('',#5335,#4266,#4267);
#3585=AXIS2_PLACEMENT_3D('',#5338,#4269,#4270);
#3586=AXIS2_PLACEMENT_3D('',#5339,#4271,#4272);
#3587=AXIS2_PLACEMENT_3D('',#5341,#4274,#4275);
#3588=AXIS2_PLACEMENT_3D('',#5343,#4277,#4278);
#3589=AXIS2_PLACEMENT_3D('',#5344,#4279,#4280);
#3590=AXIS2_PLACEMENT_3D('',#5345,#4281,#4282);
#4242=DIRECTION('axis',(0.,0.,1.));
#4243=DIRECTION('refdir',(1.,0.,0.));
#4244=DIRECTION('center_axis',(-6.12323399573548E-17,1.,4.78224871431377E-30));
#4245=DIRECTION('ref_axis',(0.939692587475203,5.75395759716863E-17,0.342020234846066));
#4246=DIRECTION('',(0.813797652501457,-0.5,0.296198211985013));
#4247=DIRECTION('center_axis',(6.12323399573548E-17,-1.,-4.78224871431377E-30));
#4248=DIRECTION('ref_axis',(0.939692587475203,5.75395759716863E-17,0.342020234846066));
#4249=DIRECTION('center_axis',(6.12323399573548E-17,-1.,-4.78224871431377E-30));
#4250=DIRECTION('ref_axis',(0.939692587475203,5.75395759716863E-17,0.342020234846066));
#4251=DIRECTION('center_axis',(-6.12323399573548E-17,1.,4.78224871431377E-30));
#4252=DIRECTION('ref_axis',(0.939692587475203,5.75395759716863E-17,0.342020234846066));
#4253=DIRECTION('',(-0.813797652501456,-0.5,-0.296198211985013));
#4254=DIRECTION('center_axis',(0.342020234846066,2.09426992923931E-17,-0.939692587475203));
#4255=DIRECTION('ref_axis',(-0.939692587475203,-5.75395759716863E-17,-0.342020234846066));
#4256=DIRECTION('',(-6.12323399573548E-17,1.,4.78224871431377E-30));
#4257=DIRECTION('',(-6.12323399573548E-17,1.,4.78224871431377E-30));
#4258=DIRECTION('center_axis',(-0.642787535078423,-3.93593848682685E-17,
-0.766044505722615));
#4259=DIRECTION('ref_axis',(-0.766044505722615,-4.6906697596874E-17,0.642787535078423));
#4260=DIRECTION('',(-6.12323399573548E-17,1.,4.78224871431377E-30));
#4261=DIRECTION('center_axis',(-0.98480776992449,-6.03020841606616E-17,
0.173648081752588));
#4262=DIRECTION('ref_axis',(0.173648081752588,1.06328783748123E-17,0.98480776992449));
#4263=DIRECTION('',(-6.12323399573548E-17,1.,4.78224871431377E-30));
#4264=DIRECTION('center_axis',(-6.12323399573548E-17,1.,4.78224871431377E-30));
#4265=DIRECTION('ref_axis',(0.939692587475203,5.75395759716863E-17,0.342020234846066));
#4266=DIRECTION('center_axis',(-6.12323399573548E-17,1.,4.78224871431377E-30));
#4267=DIRECTION('ref_axis',(0.939692587475203,5.75395759716863E-17,0.342020234846066));
#4268=DIRECTION('',(6.12323399573548E-17,-1.,-4.78224871431377E-30));
#4269=DIRECTION('center_axis',(-6.12323399573548E-17,1.,4.78224871431377E-30));
#4270=DIRECTION('ref_axis',(0.939692587475203,5.75395759716863E-17,0.342020234846066));
#4271=DIRECTION('center_axis',(-0.342020234846066,-2.09426992923931E-17,
0.939692587475203));
#4272=DIRECTION('ref_axis',(0.939692587475203,5.75395759716863E-17,0.342020234846066));
#4273=DIRECTION('',(-6.12323399573548E-17,1.,4.78224871431377E-30));
#4274=DIRECTION('center_axis',(0.98480776992449,6.03020841606616E-17,-0.173648081752589));
#4275=DIRECTION('ref_axis',(-0.173648081752589,-1.06328783748123E-17,-0.98480776992449));
#4276=DIRECTION('',(-6.12323399573548E-17,1.,4.78224871431377E-30));
#4277=DIRECTION('center_axis',(0.642787535078424,3.93593848682685E-17,0.766044505722614));
#4278=DIRECTION('ref_axis',(0.766044505722614,4.6906697596874E-17,-0.642787535078424));
#4279=DIRECTION('center_axis',(-6.12323399573548E-17,1.,4.78224871431377E-30));
#4280=DIRECTION('ref_axis',(0.939692587475203,5.75395759716863E-17,0.342020234846066));
#4281=DIRECTION('center_axis',(-6.12323399573548E-17,1.,4.78224871431377E-30));
#4282=DIRECTION('ref_axis',(0.939692587475203,5.75395759716863E-17,0.342020234846066));
#5269=CARTESIAN_POINT('',(0.,0.,0.));
#5270=CARTESIAN_POINT('Origin',(2.34923146868827,-2.18158650880638,3.85505058711526));
#5271=CARTESIAN_POINT('',(1.90695546709804,-2.18090804453173,4.22616414352457));
#5272=CARTESIAN_POINT('',(2.44948723543241,-2.18090804453173,4.42362961818127));
#5273=CARTESIAN_POINT('Ctrl Pts',(1.90695546709804,-2.18090804453173,4.22616414352457));
#5274=CARTESIAN_POINT('Ctrl Pts',(2.17822135126726,-2.2642413778637,4.32489688085366));
#5275=CARTESIAN_POINT('Ctrl Pts',(2.44948723543241,-2.18090804453173,4.42362961818127));
#5276=CARTESIAN_POINT('',(1.80669970035391,-2.18090804453173,3.65758511245857));
#5277=CARTESIAN_POINT('Ctrl Pts',(1.80669970035391,-2.18090804453173,3.65758511245857));
#5278=CARTESIAN_POINT('Ctrl Pts',(1.85682758372635,-2.2642413778637,3.9418746279937));
#5279=CARTESIAN_POINT('Ctrl Pts',(1.90695546709804,-2.18090804453173,4.22616414352457));
#5280=CARTESIAN_POINT('',(1.9028774896375,-2.24,3.69259097556336));
#5281=CARTESIAN_POINT('',(1.80780396562194,-2.18158650880638,3.65798703226866));
#5282=CARTESIAN_POINT('Origin',(2.34923146868827,-2.24,3.85505058711526));
#5283=CARTESIAN_POINT('',(2.24897570194414,-2.18090804453173,3.28647155604926));
#5284=CARTESIAN_POINT('Ctrl Pts',(2.24897570194414,-2.18090804453173,3.28647155604926));
#5285=CARTESIAN_POINT('Ctrl Pts',(2.02783770114737,-2.2642413778637,3.47202833425531));
#5286=CARTESIAN_POINT('Ctrl Pts',(1.80669970035391,-2.18090804453173,3.65758511245857));
#5287=CARTESIAN_POINT('',(2.79150747027851,-2.18090804453173,3.48393703070596));
#5288=CARTESIAN_POINT('Ctrl Pts',(2.79150747027851,-2.18090804453173,3.48393703070596));
#5289=CARTESIAN_POINT('Ctrl Pts',(2.52024158610929,-2.2642413778637,3.38520429337687));
#5290=CARTESIAN_POINT('Ctrl Pts',(2.24897570194414,-2.18090804453173,3.28647155604926));
#5291=CARTESIAN_POINT('',(2.89176323702264,-2.18090804453173,4.05251606177196));
#5292=CARTESIAN_POINT('Ctrl Pts',(2.89176323702264,-2.18090804453173,4.05251606177196));
#5293=CARTESIAN_POINT('Ctrl Pts',(2.8416353536502,-2.2642413778637,3.76822654623683));
#5294=CARTESIAN_POINT('Ctrl Pts',(2.79150747027851,-2.18090804453173,3.48393703070596));
#5295=CARTESIAN_POINT('Ctrl Pts',(2.44948723543241,-2.18090804453173,4.42362961818127));
#5296=CARTESIAN_POINT('Ctrl Pts',(2.67062523622918,-2.2642413778637,4.23807283997522));
#5297=CARTESIAN_POINT('Ctrl Pts',(2.89176323702264,-2.18090804453173,4.05251606177196));
#5298=CARTESIAN_POINT('Origin',(2.34923146868827,-1.77841349119356,3.85505058711526));
#5299=CARTESIAN_POINT('',(1.9028774896375,-1.71999999999994,3.69259097556336));
#5300=CARTESIAN_POINT('Origin',(2.34923146868827,-1.71999999999994,3.85505058711526));
#5301=CARTESIAN_POINT('',(1.80669970035391,-1.77909195546821,3.65758511245857));
#5302=CARTESIAN_POINT('',(1.80780396562194,-1.77841349119356,3.65798703226866));
#5303=CARTESIAN_POINT('',(1.90695546709804,-1.77909195546821,4.22616414352457));
#5304=CARTESIAN_POINT('Ctrl Pts',(1.90695546709804,-1.77909195546821,4.22616414352457));
#5305=CARTESIAN_POINT('Ctrl Pts',(1.8568275837256,-1.69575862213624,3.94187462798943));
#5306=CARTESIAN_POINT('Ctrl Pts',(1.80669970035391,-1.77909195546821,3.65758511245857));
#5307=CARTESIAN_POINT('',(2.44948723543241,-1.77909195546821,4.42362961818127));
#5308=CARTESIAN_POINT('Ctrl Pts',(2.44948723543241,-1.77909195546821,4.42362961818127));
#5309=CARTESIAN_POINT('Ctrl Pts',(2.17822135126319,-1.69575862213624,4.32489688085218));
#5310=CARTESIAN_POINT('Ctrl Pts',(1.90695546709804,-1.77909195546821,4.22616414352457));
#5311=CARTESIAN_POINT('',(2.89176323702264,-1.77909195546821,4.05251606177196));
#5312=CARTESIAN_POINT('Ctrl Pts',(2.89176323702264,-1.77909195546821,4.05251606177196));
#5313=CARTESIAN_POINT('Ctrl Pts',(2.67062523622586,-1.69575862213624,4.23807283997801));
#5314=CARTESIAN_POINT('Ctrl Pts',(2.44948723543241,-1.77909195546821,4.42362961818127));
#5315=CARTESIAN_POINT('',(2.79150747027851,-1.77909195546821,3.48393703070596));
#5316=CARTESIAN_POINT('Ctrl Pts',(2.79150747027851,-1.77909195546821,3.48393703070596));
#5317=CARTESIAN_POINT('Ctrl Pts',(2.84163535365095,-1.69575862213624,3.76822654624109));
#5318=CARTESIAN_POINT('Ctrl Pts',(2.89176323702264,-1.77909195546821,4.05251606177196));
#5319=CARTESIAN_POINT('',(2.24897570194414,-1.77909195546821,3.28647155604926));
#5320=CARTESIAN_POINT('Ctrl Pts',(2.24897570194414,-1.77909195546821,3.28647155604926));
#5321=CARTESIAN_POINT('Ctrl Pts',(2.52024158611336,-1.69575862213624,3.38520429337835));
#5322=CARTESIAN_POINT('Ctrl Pts',(2.79150747027851,-1.77909195546821,3.48393703070596));
#5323=CARTESIAN_POINT('Ctrl Pts',(1.80669970035391,-1.77909195546821,3.65758511245857));
#5324=CARTESIAN_POINT('Ctrl Pts',(2.02783770115069,-1.69575862213624,3.47202833425252));
#5325=CARTESIAN_POINT('Ctrl Pts',(2.24897570194414,-1.77909195546821,3.28647155604926));
#5326=CARTESIAN_POINT('Origin',(2.79150747027851,-2.24,3.48393703070596));
#5327=CARTESIAN_POINT('',(2.24897570194414,-2.24,3.28647155604926));
#5328=CARTESIAN_POINT('',(2.79150747027851,-2.24,3.48393703070596));
#5329=CARTESIAN_POINT('Origin',(2.24897570194414,-2.24,3.28647155604926));
#5330=CARTESIAN_POINT('',(1.80669970035391,-2.24,3.65758511245857));
#5331=CARTESIAN_POINT('Origin',(1.80669970035391,-2.24,3.65758511245857));
#5332=CARTESIAN_POINT('',(1.90695546709804,-2.24,4.22616414352457));
#5333=CARTESIAN_POINT('Origin',(2.34923146868827,-2.24,3.85505058711526));
#5334=CARTESIAN_POINT('',(2.11266385979137,-1.71999999999994,3.76894699299276));
#5335=CARTESIAN_POINT('Origin',(2.34923146868827,-1.71999999999994,3.85505058711526));
#5336=CARTESIAN_POINT('',(2.11266385979137,-2.24,3.76894699299276));
#5337=CARTESIAN_POINT('',(2.11266385979137,-2.24,3.76894699299276));
#5338=CARTESIAN_POINT('Origin',(2.34923146868827,-2.24,3.85505058711526));
#5339=CARTESIAN_POINT('Origin',(1.90695546709804,-2.24,4.22616414352457));
#5340=CARTESIAN_POINT('',(2.44948723543241,-2.24,4.42362961818127));
#5341=CARTESIAN_POINT('Origin',(2.89176323702264,-2.24,4.05251606177196));
#5342=CARTESIAN_POINT('',(2.89176323702264,-2.24,4.05251606177196));
#5343=CARTESIAN_POINT('Origin',(2.44948723543241,-2.24,4.42362961818127));
#5344=CARTESIAN_POINT('Origin',(2.34923146868827,-1.71999999999994,3.85505058711526));
#5345=CARTESIAN_POINT('Origin',(2.34923146868827,-2.24,3.85505058711526));
#5891=UNCERTAINTY_MEASURE_WITH_UNIT(LENGTH_MEASURE(0.001),#5930,
'DISTANCE_ACCURACY_VALUE',
'Maximum model space distance between geometric entities at asserted c
onnectivities');
#5905=UNCERTAINTY_MEASURE_WITH_UNIT(LENGTH_MEASURE(0.001),#5930,
'DISTANCE_ACCURACY_VALUE',
'Maximum model space distance between geometric entities at asserted c
onnectivities');
#5915=(
GEOMETRIC_REPRESENTATION_CONTEXT(3)
GLOBAL_UNCERTAINTY_ASSIGNED_CONTEXT((#5891))
GLOBAL_UNIT_ASSIGNED_CONTEXT((#5930,#5932,#5933))
REPRESENTATION_CONTEXT('','3D')
);
#5929=(
GEOMETRIC_REPRESENTATION_CONTEXT(3)
GLOBAL_UNCERTAINTY_ASSIGNED_CONTEXT((#5905))
GLOBAL_UNIT_ASSIGNED_CONTEXT((#5930,#5932,#5933))
REPRESENTATION_CONTEXT('','3D')
);
#5930=(
LENGTH_UNIT()
NAMED_UNIT(*)
SI_UNIT(.CENTI.,.METRE.)
);
#5932=(
NAMED_UNIT(*)
PLANE_ANGLE_UNIT()
SI_UNIT($,.RADIAN.)
);
#5933=(
NAMED_UNIT(*)
SI_UNIT($,.STERADIAN.)
SOLID_ANGLE_UNIT()
);
#5943=SHAPE_DEFINITION_REPRESENTATION(#5966,#6048);
#5966=PRODUCT_DEFINITION_SHAPE('',$,#6072);
#6048=SHAPE_REPRESENTATION('',(#3575),#5915);
#6062=PRODUCT_DEFINITION_CONTEXT('part definition',#6133,'design');
#6072=PRODUCT_DEFINITION('Hex Nut - M6','Hex Nut - M6',#6095,#6062);
#6095=PRODUCT_DEFINITION_FORMATION('',$,#6144);
#6133=APPLICATION_CONTEXT(
'Core Data for Automotive Mechanical Design Process');
#6134=PRODUCT_CONTEXT('part definition',#6133,'mechanical');
#6144=PRODUCT('Hex Nut - M6','Hex Nut - M6','Hex Nut - M6',(#6134));
#6221=COLOUR_RGB('Black',0.12,0.14,0.17);
#6222=FILL_AREA_STYLE_COLOUR('',#6221);
#6223=FILL_AREA_STYLE('',(#6222));
#6224=SURFACE_STYLE_FILL_AREA(#6223);
#6225=SURFACE_SIDE_STYLE('',(#6224));
#6226=SURFACE_STYLE_USAGE(.BOTH.,#6225);
#6227=PRESENTATION_STYLE_ASSIGNMENT((#6226));
ENDSEC;
END-ISO-10303-21;
